ISO-10303-21;
HEADER;
/* Generated by software containing ST-Developer
 * from STEP Tools, Inc. (www.steptools.com) 
 */

FILE_DESCRIPTION(
/* description */ ('Belt conveyor head drive unit'),
/* implementation_level */ '2;1');

FILE_NAME(
/* name */ 'M4 clamp nut.step',
/* time_stamp */ '2026-10-28T03:26:19-07:00',
/* author */ (''),
/* organization */ (''),
/* preprocessor_version */ 'ST-DEVELOPER v20.2',
/* originating_system */ 'Autodesk Translation Framework v15.17.0.0',
/* authorisation */ '');

FILE_SCHEMA (('AUTOMOTIVE_DESIGN { 1 0 10303 214 3 1 1 }'));
ENDSEC;

DATA;
#10=MECHANICAL_DESIGN_GEOMETRIC_PRESENTATION_REPRESENTATION('',(#855),#27069);
#717=SHAPE_REPRESENTATION_RELATIONSHIP('SRR','None',#27361,#786);
#786=ADVANCED_BREP_SHAPE_REPRESENTATION('',(#940),#27003);
#855=STYLED_ITEM('',(#27804),#940);
#940=MANIFOLD_SOLID_BREP('Body1',#13720);
#1076=FACE_BOUND('',#2636,.T.);
#1077=FACE_BOUND('',#2638,.T.);
#1348=PLANE('',#14849);
#1349=PLANE('',#14850);
#1769=FACE_OUTER_BOUND('',#2633,.T.);
#1770=FACE_OUTER_BOUND('',#2634,.T.);
#1771=FACE_OUTER_BOUND('',#2635,.T.);
#1772=FACE_OUTER_BOUND('',#2637,.T.);
#2633=EDGE_LOOP('',(#9594,#9595,#9596,#9597));
#2634=EDGE_LOOP('',(#9598,#9599,#9600,#9601));
#2635=EDGE_LOOP('',(#9602));
#2636=EDGE_LOOP('',(#9603));
#2637=EDGE_LOOP('',(#9604));
#2638=EDGE_LOOP('',(#9605));
#3682=LINE('',#21651,#4474);
#3683=LINE('',#21657,#4475);
#4474=VECTOR('',#17184,0.165);
#4475=VECTOR('',#17191,0.4);
#5216=CIRCLE('',#14844,0.165);
#5217=CIRCLE('',#14845,0.165);
#5218=CIRCLE('',#14847,0.4);
#5219=CIRCLE('',#14848,0.4);
#6165=VERTEX_POINT('',#21648);
#6166=VERTEX_POINT('',#21650);
#6167=VERTEX_POINT('',#21654);
#6168=VERTEX_POINT('',#21656);
#7489=EDGE_CURVE('',#6165,#6165,#5216,.T.);
#7490=EDGE_CURVE('',#6165,#6166,#3682,.T.);
#7491=EDGE_CURVE('',#6166,#6166,#5217,.T.);
#7492=EDGE_CURVE('',#6167,#6167,#5218,.T.);
#7493=EDGE_CURVE('',#6167,#6168,#3683,.T.);
#7494=EDGE_CURVE('',#6168,#6168,#5219,.T.);
#9594=ORIENTED_EDGE('',*,*,#7489,.F.);
#9595=ORIENTED_EDGE('',*,*,#7490,.T.);
#9596=ORIENTED_EDGE('',*,*,#7491,.T.);
#9597=ORIENTED_EDGE('',*,*,#7490,.F.);
#9598=ORIENTED_EDGE('',*,*,#7492,.F.);
#9599=ORIENTED_EDGE('',*,*,#7493,.T.);
#9600=ORIENTED_EDGE('',*,*,#7494,.T.);
#9601=ORIENTED_EDGE('',*,*,#7493,.F.);
#9602=ORIENTED_EDGE('',*,*,#7492,.T.);
#9603=ORIENTED_EDGE('',*,*,#7489,.T.);
#9604=ORIENTED_EDGE('',*,*,#7494,.F.);
#9605=ORIENTED_EDGE('',*,*,#7491,.F.);
#12597=CYLINDRICAL_SURFACE('',#14843,0.165);
#12598=CYLINDRICAL_SURFACE('',#14846,0.4);
#13048=ADVANCED_FACE('',(#1769),#12597,.F.);
#13049=ADVANCED_FACE('',(#1770),#12598,.T.);
#13050=ADVANCED_FACE('',(#1771,#1076),#1348,.T.);
#13051=ADVANCED_FACE('',(#1772,#1077),#1349,.F.);
#13720=CLOSED_SHELL('',(#13048,#13049,#13050,#13051));
#14842=AXIS2_PLACEMENT_3D('',#21646,#17178,#17179);
#14843=AXIS2_PLACEMENT_3D('',#21647,#17180,#17181);
#14844=AXIS2_PLACEMENT_3D('',#21649,#17182,#17183);
#14845=AXIS2_PLACEMENT_3D('',#21652,#17185,#17186);
#14846=AXIS2_PLACEMENT_3D('',#21653,#17187,#17188);
#14847=AXIS2_PLACEMENT_3D('',#21655,#17189,#17190);
#14848=AXIS2_PLACEMENT_3D('',#21658,#17192,#17193);
#14849=AXIS2_PLACEMENT_3D('',#21659,#17194,#17195);
#14850=AXIS2_PLACEMENT_3D('',#21660,#17196,#17197);
#17178=DIRECTION('axis',(0.,0.,1.));
#17179=DIRECTION('refdir',(1.,0.,0.));
#17180=DIRECTION('center_axis',(0.,0.,1.));
#17181=DIRECTION('ref_axis',(1.,0.,0.));
#17182=DIRECTION('center_axis',(0.,0.,-1.));
#17183=DIRECTION('ref_axis',(1.,0.,0.));
#17184=DIRECTION('',(0.,0.,-1.));
#17185=DIRECTION('center_axis',(0.,0.,-1.));
#17186=DIRECTION('ref_axis',(1.,0.,0.));
#17187=DIRECTION('center_axis',(0.,0.,1.));
#17188=DIRECTION('ref_axis',(1.,0.,0.));
#17189=DIRECTION('center_axis',(0.,0.,1.));
#17190=DIRECTION('ref_axis',(1.,0.,0.));
#17191=DIRECTION('',(0.,0.,-1.));
#17192=DIRECTION('center_axis',(0.,0.,1.));
#17193=DIRECTION('ref_axis',(1.,0.,0.));
#17194=DIRECTION('center_axis',(0.,0.,1.));
#17195=DIRECTION('ref_axis',(1.,0.,0.));
#17196=DIRECTION('center_axis',(0.,0.,1.));
#17197=DIRECTION('ref_axis',(1.,0.,0.));
#21646=CARTESIAN_POINT('',(0.,0.,0.));
#21647=CARTESIAN_POINT('Origin',(4.17091003018116,-1.,-1.6));
#21648=CARTESIAN_POINT('',(4.00591003018116,-1.,-1.2));
#21649=CARTESIAN_POINT('Origin',(4.17091003018116,-1.,-1.2));
#21650=CARTESIAN_POINT('',(4.00591003018116,-1.,-1.6));
#21651=CARTESIAN_POINT('',(4.00591003018116,-1.,-1.6));
#21652=CARTESIAN_POINT('Origin',(4.17091003018116,-1.,-1.6));
#21653=CARTESIAN_POINT('Origin',(4.17091003018116,-1.,-1.6));
#21654=CARTESIAN_POINT('',(3.77091003018116,-1.,-1.2));
#21655=CARTESIAN_POINT('Origin',(4.17091003018116,-1.,-1.2));
#21656=CARTESIAN_POINT('',(3.77091003018116,-1.,-1.6));
#21657=CARTESIAN_POINT('',(3.77091003018116,-1.,-1.6));
#21658=CARTESIAN_POINT('Origin',(4.17091003018116,-1.,-1.6));
#21659=CARTESIAN_POINT('Origin',(4.17091003018116,-1.,-1.2));
#21660=CARTESIAN_POINT('Origin',(4.17091003018116,-1.,-1.6));
#26926=UNCERTAINTY_MEASURE_WITH_UNIT(LENGTH_MEASURE(0.001),#27070,
'DISTANCE_ACCURACY_VALUE',
'Maximum model space distance between geometric entities at asserted c
onnectivities');
#26992=UNCERTAINTY_MEASURE_WITH_UNIT(LENGTH_MEASURE(0.001),#27070,
'DISTANCE_ACCURACY_VALUE',
'Maximum model space distance between geometric entities at asserted c
onnectivities');
#27003=(
GEOMETRIC_REPRESENTATION_CONTEXT(3)
GLOBAL_UNCERTAINTY_ASSIGNED_CONTEXT((#26926))
GLOBAL_UNIT_ASSIGNED_CONTEXT((#27070,#27072,#27073))
REPRESENTATION_CONTEXT('','3D')
);
#27069=(
GEOMETRIC_REPRESENTATION_CONTEXT(3)
GLOBAL_UNCERTAINTY_ASSIGNED_CONTEXT((#26992))
GLOBAL_UNIT_ASSIGNED_CONTEXT((#27070,#27072,#27073))
REPRESENTATION_CONTEXT('','3D')
);
#27070=(
LENGTH_UNIT()
NAMED_UNIT(*)
SI_UNIT(.CENTI.,.METRE.)
);
#27072=(
NAMED_UNIT(*)
PLANE_ANGLE_UNIT()
SI_UNIT($,.RADIAN.)
);
#27073=(
NAMED_UNIT(*)
SI_UNIT($,.STERADIAN.)
SOLID_ANGLE_UNIT()
);
#27084=SHAPE_DEFINITION_REPRESENTATION(#27160,#27361);
#27160=PRODUCT_DEFINITION_SHAPE('',$,#27438);
#27361=SHAPE_REPRESENTATION('',(#14842),#27003);
#27427=PRODUCT_DEFINITION_CONTEXT('part definition',#27657,'design');
#27438=PRODUCT_DEFINITION('M4 clamp nut','M4 clamp nut',#27514,#27427);
#27514=PRODUCT_DEFINITION_FORMATION('',$,#27669);
#27657=APPLICATION_CONTEXT(
'Core Data for Automotive Mechanical Design Process');
#27658=PRODUCT_CONTEXT('part definition',#27657,'mechanical');
#27669=PRODUCT('M4 clamp nut','M4 clamp nut','M4 clamp nut',(#27658));
#27798=COLOUR_RGB('Black',0.12,0.14,0.17);
#27799=FILL_AREA_STYLE_COLOUR('',#27798);
#27800=FILL_AREA_STYLE('',(#27799));
#27801=SURFACE_STYLE_FILL_AREA(#27800);
#27802=SURFACE_SIDE_STYLE('',(#27801));
#27803=SURFACE_STYLE_USAGE(.BOTH.,#27802);
#27804=PRESENTATION_STYLE_ASSIGNMENT((#27803));
ENDSEC;
END-ISO-10303-21;
